ISO-10303-21;
HEADER;
FILE_DESCRIPTION (('STEP AP214'),
    '1' );
FILE_NAME ('hex bolt gradec_iso_ISO 4016 - M8 x 40 x 22-WN.step',
    '2026-10-24T00:28:05',
    ( '' ),
    ( '' ),
    'SwSTEP 2.0',
    'SolidWorks 2025',
    '' );
FILE_SCHEMA (( 'AUTOMOTIVE_DESIGN' ));
ENDSEC;

DATA;
#12=ORIENTED_EDGE ( 'NONE', *, *, #11019, .T. ) ;
#16=FACE_OUTER_BOUND ( 'NONE', #20943, .T. ) ;
#39=ORIENTED_EDGE ( 'NONE', *, *, #13139, .T. ) ;
#42=FACE_OUTER_BOUND ( 'NONE', #15796, .T. ) ;
#48=PRODUCT_DEFINITION ( 'UNKNOWN', '', #8316, #8336 ) ;
#104=VECTOR ( 'NONE', #10753, 1000.000000000000000 ) ;
#122=ADVANCED_FACE ( 'NONE', ( #15530 ), #711, .F. ) ;
#124=CARTESIAN_POINT ( 'NONE',  ( 0.2573354458087829810, 6.889406814520511624, -1.067197363239223762 ) ) ;
#198=CARTESIAN_POINT ( 'NONE',  ( 1.395063264127832658E-15, -5.788408252967908396, -2.974182810908600150 ) ) ;
#214=DIRECTION ( 'NONE',  ( -1.000000000000000000, -0.000000000000000000, -0.000000000000000000 ) ) ;
#229=CARTESIAN_POINT ( 'NONE',  ( 5.674999999999999822, 3.752776749732560368, -6.499999999999999112 ) ) ;
#261=AXIS2_PLACEMENT_3D ( 'NONE', #1279, #21066, #12850 ) ;
#304=CARTESIAN_POINT ( 'NONE',  ( 0.000000000000000000, -5.629165124598849879, -3.250000000000003553 ) ) ;
#336=ORIENTED_EDGE ( 'NONE', *, *, #8233, .F. ) ;
#367=CARTESIAN_POINT ( 'NONE',  ( 0.000000000000000000, -5.629165124598843661, 3.250000000000012879 ) ) ;
#386=( NAMED_UNIT ( * ) PLANE_ANGLE_UNIT ( ) SI_UNIT ( $, .RADIAN. ) );
#413=DIRECTION ( 'NONE',  ( 0.000000000000000000, 0.000000000000000000, 1.000000000000000000 ) ) ;
#415=DIRECTION ( 'NONE',  ( 1.000000000000000000, 0.000000000000000000, 0.000000000000000000 ) ) ;
#469=VERTEX_POINT ( 'NONE', #13128 ) ;
#479=AXIS2_PLACEMENT_3D ( 'NONE', #7986, #1737, #16125 ) ;
#512=AXIS2_PLACEMENT_3D ( 'NONE', #229, #20006, #5182 ) ;
#530=ORIENTED_EDGE ( 'NONE', *, *, #2479, .F. ) ;
#619=CONICAL_SURFACE ( 'NONE', #12351, 3.309499999999999886, 0.7853981633974407295 ) ;
#637=LINE ( 'NONE', #11877, #10739 ) ;
#686=AXIS2_PLACEMENT_3D ( 'NONE', #15275, #2176, #3783 ) ;
#696=DIRECTION ( 'NONE',  ( 1.000000000000000000, 0.000000000000000000, 0.000000000000000000 ) ) ;
#711=PLANE ( 'NONE',  #10698 ) ;
#721=DIRECTION ( 'NONE',  ( 0.000000000000000000, 0.000000000000000000, 1.000000000000000000 ) ) ;
#741=AXIS2_PLACEMENT_3D ( 'NONE', #1558, #4786, #9334 ) ;
#768=DIRECTION ( 'NONE',  ( 0.000000000000000000, 0.000000000000000000, -1.000000000000000000 ) ) ;
#808=CARTESIAN_POINT ( 'NONE',  ( 0.000000000000000000, 0.000000000000000000, 0.000000000000000000 ) ) ;
#893=EDGE_LOOP ( 'NONE', ( #12, #19288 ) ) ;
#933=ORIENTED_EDGE ( 'NONE', *, *, #17134, .T. ) ;
#953=LINE ( 'NONE', #10873, #17064 ) ;
#957=ORIENTED_EDGE ( 'NONE', *, *, #6491, .T. ) ;
#958=EDGE_CURVE ( 'NONE', #16482, #2272, #637, .T. ) ;
#1050=ADVANCED_FACE ( 'NONE', ( #20627 ), #13825, .F. ) ;
#1071=CARTESIAN_POINT ( 'NONE',  ( 0.05533025579362307877, -6.264553569211845918, 2.149474931388140941 ) ) ;
#1111=ORIENTED_EDGE ( 'NONE', *, *, #2578, .T. ) ;
#1148=DIRECTION ( 'NONE',  ( -1.000000000000000000, -0.000000000000000000, -0.000000000000000000 ) ) ;
#1168=VECTOR ( 'NONE', #12818, 999.9999999999998863 ) ;
#1169=ORIENTED_EDGE ( 'NONE', *, *, #3622, .T. ) ;
#1179=CARTESIAN_POINT ( 'NONE',  ( 5.074999999999999289, 3.752776749732560368, -6.499999999999999112 ) ) ;
#1185=CONICAL_SURFACE ( 'NONE', #17068, 6.500000000000000000, 1.047197551196600296 ) ;
#1238=CARTESIAN_POINT ( 'NONE',  ( 5.674999999999999822, 0.000000000000000000, 0.000000000000000000 ) ) ;
#1258=ORIENTED_EDGE ( 'NONE', *, *, #20909, .F. ) ;
#1279=CARTESIAN_POINT ( 'NONE',  ( 5.074999999999999289, 0.000000000000000000, 0.000000000000000000 ) ) ;
#1358=CIRCLE ( 'NONE', #2054, 6.500000000000000888 ) ;
#1366=AXIS2_PLACEMENT_3D ( 'NONE', #21265, #13048, #3732 ) ;
#1387=CARTESIAN_POINT ( 'NONE',  ( 0.000000000000000000, 0.000000000000000000, 6.500000000000000000 ) ) ;
#1411=CARTESIAN_POINT ( 'NONE',  ( 5.074999999999999289, 3.752776749732562589, 6.500000000000000000 ) ) ;
#1418=ORIENTED_EDGE ( 'NONE', *, *, #958, .F. ) ;
#1421=DIRECTION ( 'NONE',  ( 0.000000000000000000, 0.000000000000000000, -1.000000000000000000 ) ) ;
#1438=CARTESIAN_POINT ( 'NONE',  ( 0.1061556211655336340, 6.421950209808279020, 1.876855952934451732 ) ) ;
#1451=LINE ( 'NONE', #11174, #16626 ) ;
#1463=DIRECTION ( 'NONE',  ( 1.000000000000000000, 0.000000000000000000, -0.000000000000000000 ) ) ;
#1490=B_SPLINE_CURVE_WITH_KNOTS ( 'NONE', 3,
 ( #21379, #6548, #11535, #12736, #9378, #9691 ),
 .UNSPECIFIED., .F., .F.,
 ( 4, 2, 4 ),
 ( 2.380733003139562229E-07, 0.001898835937927372897, 0.003797433802554431564 ),
 .UNSPECIFIED. ) ;
#1554=ADVANCED_FACE ( 'NONE', ( #16307 ), #14688, .F. ) ;
#1558=CARTESIAN_POINT ( 'NONE',  ( 0.000000000000000000, 0.000000000000000000, 0.000000000000000000 ) ) ;
#1571=( NAMED_UNIT ( * ) SI_UNIT ( $, .STERADIAN. ) SOLID_ANGLE_UNIT ( ) );
#1593=FACE_OUTER_BOUND ( 'NONE', #14575, .T. ) ;
#1657=UNCERTAINTY_MEASURE_WITH_UNIT (LENGTH_MEASURE( 1.000000000000000082E-05 ), #14638, 'distance_accuracy_value', 'NONE');
#1737=DIRECTION ( 'NONE',  ( -1.000000000000000000, -0.000000000000000000, -0.000000000000000000 ) ) ;
#1739=PLANE ( 'NONE',  #512 ) ;
#1758=PLANE ( 'NONE',  #686 ) ;
#1832=ORIENTED_EDGE ( 'NONE', *, *, #16714, .F. ) ;
#1884=VECTOR ( 'NONE', #12539, 1000.000000000000000 ) ;
#1887=FACE_BOUND ( 'NONE', #2376, .T. ) ;
#1934=CARTESIAN_POINT ( 'NONE',  ( 0.000000000000000000, 0.000000000000000000, 6.500000000000000888 ) ) ;
#1955=B_SPLINE_CURVE_WITH_KNOTS ( 'NONE', 3,
 ( #15011, #11532, #8271, #13051, #5037, #19970 ),
 .UNSPECIFIED., .F., .F.,
 ( 4, 2, 4 ),
 ( 0.006874058788776910706, 0.008773169699270545047, 0.01067228060976418112 ),
 .UNSPECIFIED. ) ;
#2054=AXIS2_PLACEMENT_3D ( 'NONE', #10858, #1148, #7719 ) ;
#2105=DIRECTION ( 'NONE',  ( 0.000000000000000000, -0.5000000000000009992, 0.8660254037844381525 ) ) ;
#2152=CARTESIAN_POINT ( 'NONE',  ( 5.674999999999999822, -3.752776749732576356, -6.500000000000000000 ) ) ;
#2164=EDGE_LOOP ( 'NONE', ( #7943, #957, #5762 ) ) ;
#2176=DIRECTION ( 'NONE',  ( 1.000000000000000000, 0.000000000000000000, 0.000000000000000000 ) ) ;
#2190=AXIS2_PLACEMENT_3D ( 'NONE', #13659, #13235, #5001 ) ;
#2191=EDGE_LOOP ( 'NONE', ( #4997, #14936, #2251, #12373, #1258, #8230 ) ) ;
#2217=EDGE_CURVE ( 'NONE', #2808, #12831, #9618, .T. ) ;
#2236=CARTESIAN_POINT ( 'NONE',  ( 0.5805565836007597902, 3.752776749732560368, -6.499999999999999112 ) ) ;
#2238=EDGE_CURVE ( 'NONE', #19703, #5058, #16736, .T. ) ;
#2251=ORIENTED_EDGE ( 'NONE', *, *, #5318, .F. ) ;
#2255=DIRECTION ( 'NONE',  ( 0.000000000000000000, -0.5000000000000018874, -0.8660254037844375974 ) ) ;
#2272=VERTEX_POINT ( 'NONE', #4859 ) ;
#2316=FACE_OUTER_BOUND ( 'NONE', #17897, .T. ) ;
#2376=EDGE_LOOP ( 'NONE', ( #3723, #13311 ) ) ;
#2419=DIRECTION ( 'NONE',  ( 0.000000000000000000, 0.000000000000000000, 1.000000000000000000 ) ) ;
#2428=ADVANCED_FACE ( 'NONE', ( #13415 ), #1739, .F. ) ;
#2479=EDGE_CURVE ( 'NONE', #11401, #5772, #10149, .T. ) ;
#2487=ORIENTED_EDGE ( 'NONE', *, *, #5141, .F. ) ;
#2507=DIRECTION ( 'NONE',  ( -1.000000000000000000, -0.000000000000000000, -0.000000000000000000 ) ) ;
#2526=CYLINDRICAL_SURFACE ( 'NONE', #15944, 4.000000000000000000 ) ;
#2549=LINE ( 'NONE', #10536, #104 ) ;
#2556=LINE ( 'NONE', #20834, #5748 ) ;
#2565=EDGE_CURVE ( 'NONE', #2808, #469, #20868, .T. ) ;
#2578=EDGE_CURVE ( 'NONE', #5772, #12831, #20182, .T. ) ;
#2605=FACE_OUTER_BOUND ( 'NONE', #14439, .T. ) ;
#2634=DIRECTION ( 'NONE',  ( 0.000000000000000000, 0.000000000000000000, -1.000000000000000000 ) ) ;
#2638=ORIENTED_EDGE ( 'NONE', *, *, #3136, .T. ) ;
#2717=LINE ( 'NONE', #3031, #3822 ) ;
#2747=CONICAL_SURFACE ( 'NONE', #5493, 3.309499999999999886, 0.7853981633974407295 ) ;
#2748=ORIENTED_EDGE ( 'NONE', *, *, #6180, .T. ) ;
#2768=AXIS2_PLACEMENT_3D ( 'NONE', #3557, #8303, #10033 ) ;
#2798=CARTESIAN_POINT ( 'NONE',  ( 0.2595206531159287011, 2.531175536751830268, 6.500000000000000888 ) ) ;
#2801=VECTOR ( 'NONE', #12791, 999.9999999999998863 ) ;
#2808=VERTEX_POINT ( 'NONE', #19226 ) ;
#2824=DIRECTION ( 'NONE',  ( 0.000000000000000000, 0.000000000000000000, -1.000000000000000000 ) ) ;
#2849=CARTESIAN_POINT ( 'NONE',  ( 0.01372220897661660666, 5.948365447239580384, 2.697128823393879493 ) ) ;
#2884=DIRECTION ( 'NONE',  ( 1.000000000000000000, 0.000000000000000000, 0.000000000000000000 ) ) ;
#2952=AXIS2_PLACEMENT_3D ( 'NONE', #3980, #18689, #19020 ) ;
#3031=CARTESIAN_POINT ( 'NONE',  ( 5.074999999999999289, 3.752776749732560368, -6.499999999999999112 ) ) ;
#3055=LINE ( 'NONE', #14531, #2801 ) ;
#3077=CARTESIAN_POINT ( 'NONE',  ( 44.98449999999999704, 4.898587196589412829E-16, -4.000000000000000000 ) ) ;
#3102=EDGE_CURVE ( 'NONE', #19703, #13742, #19865, .T. ) ;
#3136=EDGE_CURVE ( 'NONE', #4779, #469, #14736, .T. ) ;
#3146=ORIENTED_EDGE ( 'NONE', *, *, #7946, .T. ) ;
#3164=LINE ( 'NONE', #19916, #8179 ) ;
#3166=CARTESIAN_POINT ( 'NONE',  ( 5.674999999999999822, 0.000000000000000000, 6.500000000000000888 ) ) ;
#3174=EDGE_LOOP ( 'NONE', ( #10900, #12243, #10849, #7499, #1832, #2487 ) ) ;
#3191=CARTESIAN_POINT ( 'NONE',  ( 45.67500000000000426, 0.000000000000000000, 0.000000000000000000 ) ) ;
#3199=PLANE ( 'NONE',  #17563 ) ;
#3219=FACE_OUTER_BOUND ( 'NONE', #15290, .T. ) ;
#3228=AXIS2_PLACEMENT_3D ( 'NONE', #13866, #15600, #2824 ) ;
#3278=ORIENTED_EDGE ( 'NONE', *, *, #13849, .F. ) ;
#3323=DIRECTION ( 'NONE',  ( 0.000000000000000000, 0.000000000000000000, -1.000000000000000000 ) ) ;
#3361=EDGE_LOOP ( 'NONE', ( #7885, #12101, #1111 ) ) ;
#3370=CARTESIAN_POINT ( 'NONE',  ( -3.959031995466599785E-15, 5.309483803148794756, 3.803704290982253156 ) ) ;
#3382=ADVANCED_FACE ( 'NONE', ( #1887, #15080 ), #17011, .T. ) ;
#3389=CARTESIAN_POINT ( 'NONE',  ( -2.281271485192643599E-15, -5.469921996229795802, 3.525817189091422055 ) ) ;
#3453=CARTESIAN_POINT ( 'NONE',  ( 5.074999999999999289, 0.000000000000000000, 0.000000000000000000 ) ) ;
#3459=EDGE_LOOP ( 'NONE', ( #14362, #5481, #21306, #3548, #4004, #4975 ) ) ;
#3492=CARTESIAN_POINT ( 'NONE',  ( 5.674999999999999822, 7.505553499465139389, 0.000000000000000000 ) ) ;
#3548=ORIENTED_EDGE ( 'NONE', *, *, #13562, .F. ) ;
#3557=CARTESIAN_POINT ( 'NONE',  ( 0.000000000000000000, 0.000000000000000000, 0.000000000000000000 ) ) ;
#3594=EDGE_CURVE ( 'NONE', #5825, #17823, #13934, .T. ) ;
#3622=EDGE_CURVE ( 'NONE', #5930, #5058, #4011, .T. ) ;
#3643=B_SPLINE_CURVE_WITH_KNOTS ( 'NONE', 3,
 ( #14939, #18270, #124, #3672, #16876, #6697 ),
 .UNSPECIFIED., .F., .F.,
 ( 4, 2, 4 ),
 ( 2.380733003136581732E-07, 0.001898835937927382655, 0.003797433802554451947 ),
 .UNSPECIFIED. ) ;
#3659=DIRECTION ( 'NONE',  ( -1.000000000000000000, -0.000000000000000000, -0.000000000000000000 ) ) ;
#3667=VERTEX_POINT ( 'NONE', #10605 ) ;
#3671=ORIENTED_EDGE ( 'NONE', *, *, #12063, .T. ) ;
#3672=CARTESIAN_POINT ( 'NONE',  ( 0.05533025579362017138, 6.264553569211842365, -2.149474931388135612 ) ) ;
#3697=DIRECTION ( 'NONE',  ( 0.000000000000000000, 0.000000000000000000, 1.000000000000000000 ) ) ;
#3714=DIRECTION ( 'NONE',  ( -1.000000000000000000, -0.000000000000000000, -0.000000000000000000 ) ) ;
#3723=ORIENTED_EDGE ( 'NONE', *, *, #7317, .T. ) ;
#3732=DIRECTION ( 'NONE',  ( 0.000000000000000000, -0.5000000000000004441, 0.8660254037844383745 ) ) ;
#3773=ORIENTED_EDGE ( 'NONE', *, *, #17514, .T. ) ;
#3783=DIRECTION ( 'NONE',  ( 0.000000000000000000, 0.000000000000000000, -1.000000000000000000 ) ) ;
#3822=VECTOR ( 'NONE', #19254, 1000.000000000000000 ) ;
#3924=CARTESIAN_POINT ( 'NONE',  ( 44.98449999999999704, 0.000000000000000000, 0.000000000000000000 ) ) ;
#3929=EDGE_CURVE ( 'NONE', #5170, #5772, #14626, .T. ) ;
#3980=CARTESIAN_POINT ( 'NONE',  ( 5.074999999999999289, 0.000000000000000000, 0.000000000000000000 ) ) ;
#4004=ORIENTED_EDGE ( 'NONE', *, *, #10480, .F. ) ;
#4011=LINE ( 'NONE', #4119, #5950 ) ;
#4045=DIRECTION ( 'NONE',  ( 0.000000000000000000, 0.8660254037844375974, -0.5000000000000019984 ) ) ;
#4054=CARTESIAN_POINT ( 'NONE',  ( 45.67500000000000426, 0.000000000000000000, 0.000000000000000000 ) ) ;
#4115=ORIENTED_EDGE ( 'NONE', *, *, #14849, .T. ) ;
#4119=CARTESIAN_POINT ( 'NONE',  ( 45.67500000000000426, 0.000000000000000000, 3.309499999999999886 ) ) ;
#4144=ORIENTED_EDGE ( 'NONE', *, *, #13811, .T. ) ;
#4173=B_SPLINE_CURVE_WITH_KNOTS ( 'NONE', 3,
 ( #17861, #6287, #2849, #16259, #1438, #8007, #9215, #15836 ),
 .UNSPECIFIED., .F., .F.,
 ( 4, 2, 2, 4 ),
 ( 0.003797433802554436334, 0.004743183970586235289, 0.005688934138618035111, 0.007580434474681631285 ),
 .UNSPECIFIED. ) ;
#4187=CARTESIAN_POINT ( 'NONE',  ( 5.674999999999999822, 7.505553499465139389, 0.000000000000000000 ) ) ;
#4224=CARTESIAN_POINT ( 'NONE',  ( 5.074999999999999289, -3.752776749732576356, -6.500000000000000000 ) ) ;
#4271=AXIS2_PLACEMENT_3D ( 'NONE', #6247, #21180, #19137 ) ;
#4285=CARTESIAN_POINT ( 'NONE',  ( 5.674999999999999822, 0.000000000000000000, 0.000000000000000000 ) ) ;
#4289=VERTEX_POINT ( 'NONE', #1179 ) ;
#4401=ORIENTED_EDGE ( 'NONE', *, *, #11019, .F. ) ;
#4403=DIRECTION ( 'NONE',  ( 0.000000000000000000, 0.5000000000000008882, -0.8660254037844380415 ) ) ;
#4415=CARTESIAN_POINT ( 'NONE',  ( 5.421010862427523403E-17, 0.6351314446054991958, 6.500000000000000888 ) ) ;
#4433=DIRECTION ( 'NONE',  ( 1.000000000000000000, 0.000000000000000000, 0.000000000000000000 ) ) ;
#4474=CARTESIAN_POINT ( 'NONE',  ( 0.06682554136337748307, 4.993536075455418555, -4.350941807883111245 ) ) ;
#4519=DIRECTION ( 'NONE',  ( 0.000000000000000000, 0.000000000000000000, -1.000000000000000000 ) ) ;
#4597=CONICAL_SURFACE ( 'NONE', #3228, 6.500000000000000000, 1.047197551196600296 ) ;
#4779=VERTEX_POINT ( 'NONE', #5333 ) ;
#4783=AXIS2_PLACEMENT_3D ( 'NONE', #12303, #5374, #19802 ) ;
#4786=DIRECTION ( 'NONE',  ( 1.000000000000000000, 0.000000000000000000, -0.000000000000000000 ) ) ;
#4800=CARTESIAN_POINT ( 'NONE',  ( 5.074999999999999289, -5.629165124598850767, -3.250000000000003109 ) ) ;
#4801=VECTOR ( 'NONE', #15618, 1000.000000000000000 ) ;
#4859=CARTESIAN_POINT ( 'NONE',  ( 5.074999999999999289, -5.629165124598844550, 3.250000000000012434 ) ) ;
#4860=ORIENTED_EDGE ( 'NONE', *, *, #18010, .F. ) ;
#4901=MANIFOLD_SOLID_BREP ( 'BearingFace', #7260 ) ;
#4911=ADVANCED_FACE ( 'NONE', ( #14771 ), #8577, .T. ) ;
#4918=AXIS2_PLACEMENT_3D ( 'NONE', #7079, #14905, #413 ) ;
#4964=VECTOR ( 'NONE', #19570, 1000.000000000000000 ) ;
#4975=ORIENTED_EDGE ( 'NONE', *, *, #5721, .F. ) ;
#4997=ORIENTED_EDGE ( 'NONE', *, *, #19579, .F. ) ;
#5001=DIRECTION ( 'NONE',  ( -0.000000000000000000, 0.000000000000000000, -1.000000000000000000 ) ) ;
#5037=CARTESIAN_POINT ( 'NONE',  ( -3.557538378468059575E-17, -0.6346842323199916036, 6.500000000000000000 ) ) ;
#5052=CIRCLE ( 'NONE', #6777, 6.500000000000000888 ) ;
#5058=VERTEX_POINT ( 'NONE', #17136 ) ;
#5068=ADVANCED_FACE ( 'NONE', ( #2316 ), #2526, .T. ) ;
#5074=DIRECTION ( 'NONE',  ( 0.000000000000000000, 0.000000000000000000, 1.000000000000000000 ) ) ;
#5084=DIRECTION ( 'NONE',  ( -1.000000000000000000, -0.000000000000000000, -0.000000000000000000 ) ) ;
#5141=EDGE_CURVE ( 'NONE', #11401, #7492, #3055, .T. ) ;
#5158=DIRECTION ( 'NONE',  ( -1.000000000000000000, -0.000000000000000000, -0.000000000000000000 ) ) ;
#5170=VERTEX_POINT ( 'NONE', #9322 ) ;
#5182=DIRECTION ( 'NONE',  ( 0.000000000000000000, -0.5000000000000011102, -0.8660254037844380415 ) ) ;
#5214=CARTESIAN_POINT ( 'NONE',  ( 0.01372220897661846455, -5.309964801958114933, 3.802871176606136050 ) ) ;
#5249=EDGE_LOOP ( 'NONE', ( #14465, #11892, #11024, #7834, #10874, #11376 ) ) ;
#5310=ORIENTED_EDGE ( 'NONE', *, *, #6130, .T. ) ;
#5318=EDGE_CURVE ( 'NONE', #14150, #10771, #4173, .T. ) ;
#5333=CARTESIAN_POINT ( 'NONE',  ( 0.000000000000000000, -5.629165124598849879, -3.250000000000003553 ) ) ;
#5357=LINE ( 'NONE', #10327, #18685 ) ;
#5368=FACE_OUTER_BOUND ( 'NONE', #18444, .T. ) ;
#5374=DIRECTION ( 'NONE',  ( -1.000000000000000000, -0.000000000000000000, -0.000000000000000000 ) ) ;
#5479=CYLINDRICAL_SURFACE ( 'NONE', #9684, 6.500000000000000888 ) ;
#5481=ORIENTED_EDGE ( 'NONE', *, *, #10278, .T. ) ;
#5493=AXIS2_PLACEMENT_3D ( 'NONE', #12996, #8220, #14848 ) ;
#5511=VECTOR ( 'NONE', #3659, 1000.000000000000000 ) ;
#5594=CARTESIAN_POINT ( 'NONE',  ( 0.5805565836007611225, 3.752776749732563033, 6.500000000000000000 ) ) ;
#5669=VERTEX_POINT ( 'NONE', #7563 ) ;
#5721=EDGE_CURVE ( 'NONE', #5772, #4289, #2717, .T. ) ;
#5748=VECTOR ( 'NONE', #10439, 999.9999999999998863 ) ;
#5762=ORIENTED_EDGE ( 'NONE', *, *, #17681, .T. ) ;
#5772=VERTEX_POINT ( 'NONE', #11021 ) ;
#5825=VERTEX_POINT ( 'NONE', #11565 ) ;
#5849=CARTESIAN_POINT ( 'NONE',  ( 0.4042117618284690184, -3.141900367810046557, -6.499999999999999112 ) ) ;
#5859=AXIS2_PLACEMENT_3D ( 'NONE', #13578, #20167, #11934 ) ;
#5889=CARTESIAN_POINT ( 'NONE',  ( 5.074999999999999289, 7.505553499465139389, 0.000000000000000000 ) ) ;
#5930=VERTEX_POINT ( 'NONE', #16444 ) ;
#5941=DIRECTION ( 'NONE',  ( 0.000000000000000000, 0.000000000000000000, -1.000000000000000000 ) ) ;
#5950=VECTOR ( 'NONE', #17223, 999.9999999999998863 ) ;
#5952=ORIENTED_EDGE ( 'NONE', *, *, #7317, .F. ) ;
#6033=EDGE_CURVE ( 'NONE', #3667, #20822, #18879, .T. ) ;
#6130=EDGE_CURVE ( 'NONE', #12049, #11027, #17096, .T. ) ;
#6135=CARTESIAN_POINT ( 'NONE',  ( 0.5805565836007611225, 3.752776749732563033, 6.500000000000000000 ) ) ;
#6168=ADVANCED_FACE ( 'NONE', ( #42 ), #15180, .F. ) ;
#6177=DIRECTION ( 'NONE',  ( 0.000000000000000000, -1.000000000000000000, 0.000000000000000000 ) ) ;
#6180=EDGE_CURVE ( 'NONE', #13749, #14150, #8739, .T. ) ;
#6237=CARTESIAN_POINT ( 'NONE',  ( 5.674999999999999822, 3.752776749732562589, 6.500000000000000000 ) ) ;
#6247=CARTESIAN_POINT ( 'NONE',  ( 5.074999999999999289, 6.500000000000000888, 0.000000000000000000 ) ) ;
#6263=CYLINDRICAL_SURFACE ( 'NONE', #479, 6.500000000000000888 ) ;
#6270=ORIENTED_EDGE ( 'NONE', *, *, #14849, .F. ) ;
#6287=CARTESIAN_POINT ( 'NONE',  ( -3.933621007048970775E-15, 5.788408252967900403, 2.974182810908597485 ) ) ;
#6315=DIRECTION ( 'NONE',  ( -0.000000000000000000, 0.000000000000000000, 1.000000000000000000 ) ) ;
#6346=VECTOR ( 'NONE', #6766, 1000.000000000000000 ) ;
#6348=EDGE_CURVE ( 'NONE', #5058, #15419, #8984, .T. ) ;
#6352=VERTEX_POINT ( 'NONE', #9091 ) ;
#6367=FACE_OUTER_BOUND ( 'NONE', #14070, .T. ) ;
#6369=DIRECTION ( 'NONE',  ( -1.000000000000000000, -0.000000000000000000, -0.000000000000000000 ) ) ;
#6467=CIRCLE ( 'NONE', #12006, 6.500000000000000888 ) ;
#6491=EDGE_CURVE ( 'NONE', #10771, #3667, #3643, .T. ) ;
#6505=ORIENTED_EDGE ( 'NONE', *, *, #12118, .F. ) ;
#6548=CARTESIAN_POINT ( 'NONE',  ( 0.4033376246892518835, -4.059728990630810941, -5.968343123267134231 ) ) ;
#6590=CARTESIAN_POINT ( 'NONE',  ( 0.000000000000000000, 0.000000000000000000, 0.000000000000000000 ) ) ;
#6593=MECHANICAL_DESIGN_GEOMETRIC_PRESENTATION_REPRESENTATION('',(#15253),#15206);
#6682=LINE ( 'NONE', #2152, #5511 ) ;
#6697=CARTESIAN_POINT ( 'NONE',  ( 0.000000000000000000, 5.629165124598846326, -3.250000000000007550 ) ) ;
#6708=ADVANCED_FACE ( 'NONE', ( #7968 ), #20870, .T. ) ;
#6719=DIRECTION ( 'NONE',  ( 1.000000000000000000, 0.000000000000000000, 0.000000000000000000 ) ) ;
#6743=CARTESIAN_POINT ( 'NONE',  ( 0.000000000000000000, 0.000000000000000000, 0.000000000000000000 ) ) ;
#6766=DIRECTION ( 'NONE',  ( -1.000000000000000000, -0.000000000000000000, -0.000000000000000000 ) ) ;
#6777=AXIS2_PLACEMENT_3D ( 'NONE', #7800, #17658, #10840 ) ;
#6789=DIRECTION ( 'NONE',  ( 0.000000000000000000, -1.000000000000000000, -1.155626614413199331E-16 ) ) ;
#6872=CARTESIAN_POINT ( 'NONE',  ( 0.4037800551813791605, -7.199367570657613236, -0.5303295852573151059 ) ) ;
#6938=DIRECTION ( 'NONE',  ( -0.000000000000000000, 0.000000000000000000, -1.000000000000000000 ) ) ;
#6954=DIRECTION ( 'NONE',  ( -1.000000000000000000, -0.000000000000000000, -0.000000000000000000 ) ) ;
#7057=CARTESIAN_POINT ( 'NONE',  ( 5.074999999999999289, 7.505553499465139389, 0.000000000000000000 ) ) ;
#7079=CARTESIAN_POINT ( 'NONE',  ( 45.67500000000000426, 0.000000000000000000, 0.000000000000000000 ) ) ;
#7260=CLOSED_SHELL ( 'NONE', ( #18867, #17030, #4911, #3382, #5068, #9607, #16001, #19201, #9611, #12315, #6708, #9995, #7668, #11293, #6168, #18655, #10599, #18430, #10265, #18334, #20210, #10260, #1554, #122, #17813, #1050, #2428 ) ) ;
#7277=ORIENTED_EDGE ( 'NONE', *, *, #7539, .F. ) ;
#7283=DIRECTION ( 'NONE',  ( 0.000000000000000000, 0.5000000000000018874, 0.8660254037844374864 ) ) ;
#7314=CARTESIAN_POINT ( 'NONE',  ( 0.2573354458087815932, 4.368923434677187245, 5.432802636760778903 ) ) ;
#7317=EDGE_CURVE ( 'NONE', #15419, #13742, #9453, .T. ) ;
#7333=CARTESIAN_POINT ( 'NONE',  ( 0.5805565836007606784, -3.752776749732561701, 6.500000000000000000 ) ) ;
#7432=UNCERTAINTY_MEASURE_WITH_UNIT (LENGTH_MEASURE( 1.000000000000000082E-05 ), #16819, 'distance_accuracy_value', 'NONE');
#7442=ORIENTED_EDGE ( 'NONE', *, *, #20909, .T. ) ;
#7463=CARTESIAN_POINT ( 'NONE',  ( 0.000000000000000000, 7.511572993685794170E-16, -6.499999999999999112 ) ) ;
#7485=APPLICATION_CONTEXT ( 'automotive_design' ) ;
#7492=VERTEX_POINT ( 'NONE', #9143 ) ;
#7499=ORIENTED_EDGE ( 'NONE', *, *, #6491, .F. ) ;
#7539=EDGE_CURVE ( 'NONE', #6352, #16482, #953, .T. ) ;
#7563=CARTESIAN_POINT ( 'NONE',  ( 5.674999999999999822, 7.960204194457796463E-16, -6.500000000000000888 ) ) ;
#7574=AXIS2_PLACEMENT_3D ( 'NONE', #17521, #15698, #5941 ) ;
#7641=CARTESIAN_POINT ( 'NONE',  ( 0.000000000000000000, -5.629165124598843661, 3.250000000000012879 ) ) ;
#7651=CARTESIAN_POINT ( 'NONE',  ( 0.000000000000000000, 0.000000000000000000, 6.500000000000000000 ) ) ;
#7668=ADVANCED_FACE ( 'NONE', ( #18005 ), #3199, .T. ) ;
#7708=CARTESIAN_POINT ( 'NONE',  ( 0.4037800551813705008, 4.058962678540093627, -5.969670414742685338 ) ) ;
#7714=ORIENTED_EDGE ( 'NONE', *, *, #2479, .T. ) ;
#7719=DIRECTION ( 'NONE',  ( 0.000000000000000000, 0.000000000000000000, 1.000000000000000000 ) ) ;
#7800=CARTESIAN_POINT ( 'NONE',  ( 0.000000000000000000, 0.000000000000000000, 0.000000000000000000 ) ) ;
#7834=ORIENTED_EDGE ( 'NONE', *, *, #20524, .F. ) ;
#7885=ORIENTED_EDGE ( 'NONE', *, *, #20200, .T. ) ;
#7911=ORIENTED_EDGE ( 'NONE', *, *, #5141, .T. ) ;
#7943=ORIENTED_EDGE ( 'NONE', *, *, #5318, .T. ) ;
#7946=EDGE_CURVE ( 'NONE', #13150, #11401, #18583, .T. ) ;
#7968=FACE_OUTER_BOUND ( 'NONE', #10899, .T. ) ;
#7980=AXIS2_PLACEMENT_3D ( 'NONE', #19345, #17302, #768 ) ;
#7986=CARTESIAN_POINT ( 'NONE',  ( 0.000000000000000000, 0.000000000000000000, 0.000000000000000000 ) ) ;
#8007=CARTESIAN_POINT ( 'NONE',  ( 0.2578475836320706649, 6.890627091270370208, 1.065083781909172966 ) ) ;
#8008=CARTESIAN_POINT ( 'NONE',  ( 0.000000000000000000, 7.511572993685794170E-16, -6.499999999999999112 ) ) ;
#8013=EDGE_CURVE ( 'NONE', #13314, #14150, #16606, .T. ) ;
#8019=PRODUCT ( 'hex bolt gradec_iso_ISO 4016 - M8 x 40 x 22-WN', 'hex bolt gradec_iso_ISO 4016 - M8 x 40 x 22-WN', '', ( #14978 ) ) ;
#8038=FACE_OUTER_BOUND ( 'NONE', #16777, .T. ) ;
#8096=ORIENTED_EDGE ( 'NONE', *, *, #12661, .T. ) ;
#8123=CARTESIAN_POINT ( 'NONE',  ( 0.01372220897661549643, 5.309964801958114045, -3.802871176606129833 ) ) ;
#8179=VECTOR ( 'NONE', #18076, 1000.000000000000000 ) ;
#8220=DIRECTION ( 'NONE',  ( -1.000000000000000000, -0.000000000000000000, -0.000000000000000000 ) ) ;
#8230=ORIENTED_EDGE ( 'NONE', *, *, #16371, .F. ) ;
#8233=EDGE_CURVE ( 'NONE', #469, #12049, #15306, .T. ) ;
#8263=ORIENTED_EDGE ( 'NONE', *, *, #8780, .F. ) ;
#8271=CARTESIAN_POINT ( 'NONE',  ( 0.2565376335220200255, -2.516992571281979618, 6.500000000000000888 ) ) ;
#8289=EDGE_CURVE ( 'NONE', #11027, #13749, #1955, .T. ) ;
#8303=DIRECTION ( 'NONE',  ( 1.000000000000000000, 0.000000000000000000, 0.000000000000000000 ) ) ;
#8316=PRODUCT_DEFINITION_FORMATION_WITH_SPECIFIED_SOURCE ( 'ANY', '', #8019, .NOT_KNOWN. ) ;
#8321=LINE ( 'NONE', #9626, #10054 ) ;
#8336=PRODUCT_DEFINITION_CONTEXT ( 'detailed design', #7485, 'design' ) ;
#8337=FACE_OUTER_BOUND ( 'NONE', #16454, .T. ) ;
#8340=CONICAL_SURFACE ( 'NONE', #18011, 6.500000000000000000, 1.047197551196600296 ) ;
#8345=CARTESIAN_POINT ( 'NONE',  ( 0.1061556211655345777, -4.836380039389415408, 4.623144047065558482 ) ) ;
#8453=CARTESIAN_POINT ( 'NONE',  ( 0.2578475836320701653, -4.367703157927325996, 5.434916218090832807 ) ) ;
#8462=SHAPE_DEFINITION_REPRESENTATION ( #21163, #8616 ) ;
#8495=CARTESIAN_POINT ( 'NONE',  ( 0.1061556211655389631, -6.421950209808288790, -1.876855952934453731 ) ) ;
#8508=CIRCLE ( 'NONE', #13700, 4.000000000000000000 ) ;
#8519=CARTESIAN_POINT ( 'NONE',  ( 5.674999999999999822, 3.752776749732560368, -6.499999999999999112 ) ) ;
#8559=CARTESIAN_POINT ( 'NONE',  ( 0.4037800551813712224, -4.058962678540093627, 5.969670414742685338 ) ) ;
#8560=ORIENTED_EDGE ( 'NONE', *, *, #6348, .F. ) ;
#8577=CYLINDRICAL_SURFACE ( 'NONE', #5859, 4.000000000000000000 ) ;
#8616=SHAPE_REPRESENTATION ( 'hex bolt gradec_iso_ISO 4016 - M8 x 40 x 22-WN', ( #12794 ), #13835 ) ;
#8658=EDGE_LOOP ( 'NONE', ( #9448, #39, #13231 ) ) ;
#8739=CIRCLE ( 'NONE', #15328, 6.500000000000000000 ) ;
#8776=ORIENTED_EDGE ( 'NONE', *, *, #7539, .T. ) ;
#8780=EDGE_CURVE ( 'NONE', #2272, #6352, #1358, .T. ) ;
#8802=ORIENTED_EDGE ( 'NONE', *, *, #8289, .F. ) ;
#8843=CIRCLE ( 'NONE', #19564, 6.500000000000000888 ) ;
#8847=AXIS2_PLACEMENT_3D ( 'NONE', #18079, #6719, #14356 ) ;
#8896=CARTESIAN_POINT ( 'NONE',  ( 0.000000000000000000, 0.000000000000000000, 0.000000000000000000 ) ) ;
#8912=ORIENTED_EDGE ( 'NONE', *, *, #17514, .F. ) ;
#8939=VECTOR ( 'NONE', #6177, 1000.000000000000000 ) ;
#8973=CARTESIAN_POINT ( 'NONE',  ( 0.000000000000000000, 7.960204194457796463E-16, -6.500000000000000888 ) ) ;
#8984=LINE ( 'NONE', #17323, #20843 ) ;
#9016=CARTESIAN_POINT ( 'NONE',  ( 5.674999999999999822, -7.505553499465148271, 0.000000000000000000 ) ) ;
#9039=CIRCLE ( 'NONE', #7980, 6.500000000000000888 ) ;
#9091=CARTESIAN_POINT ( 'NONE',  ( 5.074999999999999289, 0.000000000000000000, 6.500000000000000888 ) ) ;
#9143=CARTESIAN_POINT ( 'NONE',  ( 5.074999999999999289, 7.505553499465139389, 0.000000000000000000 ) ) ;
#9215=CARTESIAN_POINT ( 'NONE',  ( 0.4037800551813744421, 7.199367570657605242, 0.5303295852573141067 ) ) ;
#9234=ORIENTED_EDGE ( 'NONE', *, *, #16099, .F. ) ;
#9237=EDGE_CURVE ( 'NONE', #16482, #11027, #17234, .T. ) ;
#9253=ORIENTED_EDGE ( 'NONE', *, *, #8013, .T. ) ;
#9265=CARTESIAN_POINT ( 'NONE',  ( 0.4033376246892542705, -7.198601258566906580, 0.5316568767328695433 ) ) ;
#9308=AXIS2_PLACEMENT_3D ( 'NONE', #8519, #18257, #6789 ) ;
#9319=( NAMED_UNIT ( * ) PLANE_ANGLE_UNIT ( ) SI_UNIT ( $, .RADIAN. ) );
#9322=CARTESIAN_POINT ( 'NONE',  ( 5.074999999999999289, -3.752776749732576800, -6.500000000000000000 ) ) ;
#9323=CARTESIAN_POINT ( 'NONE',  ( 5.674999999999999822, 0.000000000000000000, 0.000000000000000000 ) ) ;
#9334=DIRECTION ( 'NONE',  ( 0.000000000000000000, 0.000000000000000000, -1.000000000000000000 ) ) ;
#9361=EDGE_CURVE ( 'NONE', #18908, #6352, #17758, .T. ) ;
#9378=CARTESIAN_POINT ( 'NONE',  ( 1.521271173268723212E-15, -5.309483803148806302, -3.803704290982254932 ) ) ;
#9384=CARTESIAN_POINT ( 'NONE',  ( 0.4053525175235891398, 3.145852061455925774, 6.499999999999999112 ) ) ;
#9436=AXIS2_PLACEMENT_3D ( 'NONE', #16522, #9793, #16415 ) ;
#9441=CARTESIAN_POINT ( 'NONE',  ( 0.2578475836320677783, 4.367703157927326885, -5.434916218090831030 ) ) ;
#9448=ORIENTED_EDGE ( 'NONE', *, *, #20524, .T. ) ;
#9453=CIRCLE ( 'NONE', #17742, 4.000000000000000000 ) ;
#9500=ORIENTED_EDGE ( 'NONE', *, *, #2238, .F. ) ;
#9584=CARTESIAN_POINT ( 'NONE',  ( 0.5805565836007702263, -7.505553499465148271, -1.692530754021427292E-16 ) ) ;
#9607=ADVANCED_FACE ( 'NONE', ( #14636 ), #2747, .T. ) ;
#9611=ADVANCED_FACE ( 'NONE', ( #16573 ), #1758, .T. ) ;
#9618=LINE ( 'NONE', #11136, #4964 ) ;
#9626=CARTESIAN_POINT ( 'NONE',  ( 5.674999999999999822, 3.752776749732560368, -6.499999999999999112 ) ) ;
#9684=AXIS2_PLACEMENT_3D ( 'NONE', #20203, #214, #15450 ) ;
#9691=CARTESIAN_POINT ( 'NONE',  ( 0.000000000000000000, -5.629165124598849879, -3.250000000000003553 ) ) ;
#9767=CARTESIAN_POINT ( 'NONE',  ( 45.67500000000000426, 4.475777889183788807E-16, -3.309499999999999886 ) ) ;
#9793=DIRECTION ( 'NONE',  ( 1.000000000000000000, 0.000000000000000000, 0.000000000000000000 ) ) ;
#9847=CARTESIAN_POINT ( 'NONE',  ( 0.4053525175236805667, 3.145852061456244630, -6.500000000000000000 ) ) ;
#9884=EDGE_LOOP ( 'NONE', ( #6505, #18999, #1169, #9500 ) ) ;
#9911=CIRCLE ( 'NONE', #18547, 3.309499999999999886 ) ;
#9995=ADVANCED_FACE ( 'NONE', ( #20556 ), #12331, .T. ) ;
#10033=DIRECTION ( 'NONE',  ( 0.000000000000000000, 0.000000000000000000, -1.000000000000000000 ) ) ;
#10038=DIRECTION ( 'NONE',  ( 0.000000000000000000, 0.000000000000000000, 1.000000000000000000 ) ) ;
#10054=VECTOR ( 'NONE', #5084, 1000.000000000000000 ) ;
#10077=DIRECTION ( 'NONE',  ( 1.000000000000000000, 0.000000000000000000, -0.000000000000000000 ) ) ;
#10120=CARTESIAN_POINT ( 'NONE',  ( 0.06682554136338426931, -6.264794173742287420, -2.149058192116898081 ) ) ;
#10149=CIRCLE ( 'NONE', #12586, 6.500000000000000888 ) ;
#10260=ADVANCED_FACE ( 'NONE', ( #18471 ), #13622, .F. ) ;
#10265=ADVANCED_FACE ( 'NONE', ( #19887 ), #11033, .T. ) ;
#10268=VECTOR ( 'NONE', #15702, 1000.000000000000000 ) ;
#10278=EDGE_CURVE ( 'NONE', #5170, #17823, #6682, .T. ) ;
#10299=DIRECTION ( 'NONE',  ( 0.000000000000000000, 0.000000000000000000, 1.000000000000000000 ) ) ;
#10301=DIRECTION ( 'NONE',  ( 1.000000000000000000, 0.000000000000000000, -0.000000000000000000 ) ) ;
#10327=CARTESIAN_POINT ( 'NONE',  ( 5.074999999999999289, -7.505553499465148271, 0.000000000000000000 ) ) ;
#10439=DIRECTION ( 'NONE',  ( -0.000000000000000000, 0.5000000000000012212, 0.8660254037844380415 ) ) ;
#10480=EDGE_CURVE ( 'NONE', #4289, #20822, #8321, .T. ) ;
#10514=CARTESIAN_POINT ( 'NONE',  ( 0.000000000000000000, 0.000000000000000000, 0.000000000000000000 ) ) ;
#10536=CARTESIAN_POINT ( 'NONE',  ( 5.674999999999999822, 3.752776749732562589, 6.500000000000000000 ) ) ;
#10590=AXIS2_PLACEMENT_3D ( 'NONE', #3924, #6954, #10299 ) ;
#10599=ADVANCED_FACE ( 'NONE', ( #16 ), #8340, .T. ) ;
#10604=ORIENTED_EDGE ( 'NONE', *, *, #13849, .T. ) ;
#10605=CARTESIAN_POINT ( 'NONE',  ( 0.000000000000000000, 5.629165124598846326, -3.250000000000007550 ) ) ;
#10698=AXIS2_PLACEMENT_3D ( 'NONE', #9016, #4045, #7283 ) ;
#10739=VECTOR ( 'NONE', #2255, 999.9999999999998863 ) ;
#10753=DIRECTION ( 'NONE',  ( -1.000000000000000000, -0.000000000000000000, -0.000000000000000000 ) ) ;
#10771=VERTEX_POINT ( 'NONE', #11895 ) ;
#10838=CARTESIAN_POINT ( 'NONE',  ( 5.074999999999999289, -3.752776749732561257, 6.500000000000000000 ) ) ;
#10840=DIRECTION ( 'NONE',  ( 0.000000000000000000, 0.000000000000000000, -1.000000000000000000 ) ) ;
#10849=ORIENTED_EDGE ( 'NONE', *, *, #6033, .F. ) ;
#10858=CARTESIAN_POINT ( 'NONE',  ( 5.074999999999999289, 0.000000000000000000, 0.000000000000000000 ) ) ;
#10860=LINE ( 'NONE', #5889, #1168 ) ;
#10873=CARTESIAN_POINT ( 'NONE',  ( 5.074999999999999289, 3.752776749732562589, 6.500000000000000000 ) ) ;
#10874=ORIENTED_EDGE ( 'NONE', *, *, #10278, .F. ) ;
#10892=DIRECTION ( 'NONE',  ( 0.000000000000000000, 0.000000000000000000, -1.000000000000000000 ) ) ;
#10899=EDGE_LOOP ( 'NONE', ( #8776, #19107, #18822 ) ) ;
#10900=ORIENTED_EDGE ( 'NONE', *, *, #18151, .F. ) ;
#11019=EDGE_CURVE ( 'NONE', #13344, #5669, #9039, .T. ) ;
#11021=CARTESIAN_POINT ( 'NONE',  ( 5.074999999999999289, 7.511572993685795156E-16, -6.500000000000000000 ) ) ;
#11024=ORIENTED_EDGE ( 'NONE', *, *, #3136, .F. ) ;
#11027=VERTEX_POINT ( 'NONE', #7333 ) ;
#11033=CONICAL_SURFACE ( 'NONE', #2768, 6.500000000000000000, 1.047197551196600296 ) ;
#11064=ORIENTED_EDGE ( 'NONE', *, *, #2565, .F. ) ;
#11136=CARTESIAN_POINT ( 'NONE',  ( 5.074999999999999289, -3.752776749732576356, -6.500000000000000000 ) ) ;
#11174=CARTESIAN_POINT ( 'NONE',  ( 45.67500000000000426, 4.052968581778165278E-16, -3.309499999999999886 ) ) ;
#11290=PLANE ( 'NONE',  #16845 ) ;
#11293=ADVANCED_FACE ( 'NONE', ( #5368 ), #5479, .T. ) ;
#11317=B_SPLINE_CURVE_WITH_KNOTS ( 'NONE', 3,
 ( #19815, #9847, #18183, #19918, #16260, #8008 ),
 .UNSPECIFIED., .F., .F.,
 ( 4, 2, 4 ),
 ( 0.01913986446880883499, 0.02104055318064342039, 0.02294124189247800580 ),
 .UNSPECIFIED. ) ;
#11321=PLANE ( 'NONE',  #12664 ) ;
#11376=ORIENTED_EDGE ( 'NONE', *, *, #20200, .F. ) ;
#11401=VERTEX_POINT ( 'NONE', #11874 ) ;
#11413=CIRCLE ( 'NONE', #741, 6.500000000000000888 ) ;
#11423=PLANE ( 'NONE',  #14914 ) ;
#11532=CARTESIAN_POINT ( 'NONE',  ( 0.4042117618287672243, -3.141900367811076400, 6.500000000000000000 ) ) ;
#11535=CARTESIAN_POINT ( 'NONE',  ( 0.2573354458087862007, -4.368923434677201456, -5.432802636760778903 ) ) ;
#11541=FACE_OUTER_BOUND ( 'NONE', #11687, .T. ) ;
#11565=CARTESIAN_POINT ( 'NONE',  ( 0.000000000000000000, 7.511572993685794170E-16, -6.499999999999999112 ) ) ;
#11625=CIRCLE ( 'NONE', #16126, 6.500000000000000888 ) ;
#11642=CARTESIAN_POINT ( 'NONE',  ( 0.000000000000000000, 4.898587196589412829E-16, -4.000000000000000000 ) ) ;
#11687=EDGE_LOOP ( 'NONE', ( #18115, #7442, #20569, #8802, #14176, #7277 ) ) ;
#11858=CARTESIAN_POINT ( 'NONE',  ( 5.074999999999999289, 6.500000000000000888, 0.000000000000000000 ) ) ;
#11874=CARTESIAN_POINT ( 'NONE',  ( 5.074999999999999289, 5.629165124598847214, -3.250000000000007550 ) ) ;
#11877=CARTESIAN_POINT ( 'NONE',  ( 5.074999999999999289, -7.505553499465148271, 0.000000000000000000 ) ) ;
#11889=EDGE_LOOP ( 'NONE', ( #8096, #14343, #10604 ) ) ;
#11891=ORIENTED_EDGE ( 'NONE', *, *, #13055, .T. ) ;
#11892=ORIENTED_EDGE ( 'NONE', *, *, #2565, .T. ) ;
#11895=CARTESIAN_POINT ( 'NONE',  ( 0.5805565836007647862, 7.505553499465139389, 2.227827669841787811E-16 ) ) ;
#11934=DIRECTION ( 'NONE',  ( 0.000000000000000000, 0.000000000000000000, 1.000000000000000000 ) ) ;
#11967=ORIENTED_EDGE ( 'NONE', *, *, #9237, .T. ) ;
#11987=DIRECTION ( 'NONE',  ( -1.000000000000000000, -0.000000000000000000, -0.000000000000000000 ) ) ;
#12006=AXIS2_PLACEMENT_3D ( 'NONE', #3453, #11987, #10038 ) ;
#12037=LINE ( 'NONE', #7057, #13387 ) ;
#12049=VERTEX_POINT ( 'NONE', #12915 ) ;
#12063=EDGE_CURVE ( 'NONE', #13749, #12049, #11413, .T. ) ;
#12101=ORIENTED_EDGE ( 'NONE', *, *, #3929, .T. ) ;
#12118=EDGE_CURVE ( 'NONE', #21094, #19703, #1451, .T. ) ;
#12197=CARTESIAN_POINT ( 'NONE',  ( 0.000000000000000000, 5.629165124598848102, 3.250000000000005329 ) ) ;
#12243=ORIENTED_EDGE ( 'NONE', *, *, #10480, .T. ) ;
#12259=DIRECTION ( 'NONE',  ( 0.000000000000000000, 0.000000000000000000, 1.000000000000000000 ) ) ;
#12303=CARTESIAN_POINT ( 'NONE',  ( 5.074999999999999289, 0.000000000000000000, 0.000000000000000000 ) ) ;
#12315=ADVANCED_FACE ( 'NONE', ( #3219 ), #11423, .T. ) ;
#12331=PLANE ( 'NONE',  #7574 ) ;
#12348=CARTESIAN_POINT ( 'NONE',  ( 0.05458999538772797006, -1.264741368073337480, -6.500000000000000888 ) ) ;
#12351=AXIS2_PLACEMENT_3D ( 'NONE', #18923, #19042, #17316 ) ;
#12373=ORIENTED_EDGE ( 'NONE', *, *, #8013, .F. ) ;
#12433=ORIENTED_EDGE ( 'NONE', *, *, #3102, .F. ) ;
#12476=CARTESIAN_POINT ( 'NONE',  ( 5.074999999999999289, 5.629165124598848990, 3.250000000000006217 ) ) ;
#12517=ORIENTED_EDGE ( 'NONE', *, *, #13055, .F. ) ;
#12539=DIRECTION ( 'NONE',  ( -1.000000000000000000, -0.000000000000000000, -0.000000000000000000 ) ) ;
#12586=AXIS2_PLACEMENT_3D ( 'NONE', #15258, #20217, #5074 ) ;
#12601=ORIENTED_EDGE ( 'NONE', *, *, #6130, .F. ) ;
#12632=CARTESIAN_POINT ( 'NONE',  ( -2.371692252312040949E-15, -5.948846446048902337, 2.696295709017763276 ) ) ;
#12656=CARTESIAN_POINT ( 'NONE',  ( 0.000000000000000000, 0.000000000000000000, 0.000000000000000000 ) ) ;
#12661=EDGE_CURVE ( 'NONE', #2272, #2808, #5357, .T. ) ;
#12664=AXIS2_PLACEMENT_3D ( 'NONE', #6237, #4519, #14381 ) ;
#12736=CARTESIAN_POINT ( 'NONE',  ( 0.05533025579362575719, -4.993776679985864497, -4.350525068611871049 ) ) ;
#12791=DIRECTION ( 'NONE',  ( -0.000000000000000000, 0.5000000000000012212, 0.8660254037844380415 ) ) ;
#12794=AXIS2_PLACEMENT_3D ( 'NONE', #808, #2419, #696 ) ;
#12818=DIRECTION ( 'NONE',  ( 0.000000000000000000, -0.5000000000000009992, 0.8660254037844381525 ) ) ;
#12831=VERTEX_POINT ( 'NONE', #4800 ) ;
#12850=DIRECTION ( 'NONE',  ( 0.000000000000000000, 0.000000000000000000, 1.000000000000000000 ) ) ;
#12884=ORIENTED_EDGE ( 'NONE', *, *, #16371, .T. ) ;
#12915=CARTESIAN_POINT ( 'NONE',  ( 0.000000000000000000, -5.629165124598843661, 3.250000000000012879 ) ) ;
#12938=CARTESIAN_POINT ( 'NONE',  ( 5.074999999999999289, 6.500000000000000888, 0.000000000000000000 ) ) ;
#12996=CARTESIAN_POINT ( 'NONE',  ( 45.67500000000000426, 0.000000000000000000, 0.000000000000000000 ) ) ;
#13000=AXIS2_PLACEMENT_3D ( 'NONE', #13115, #15973, #13337 ) ;
#13014=CIRCLE ( 'NONE', #17506, 6.500000000000000888 ) ;
#13048=DIRECTION ( 'NONE',  ( -0.000000000000000000, 0.8660254037844383745, 0.5000000000000004441 ) ) ;
#13051=CARTESIAN_POINT ( 'NONE',  ( 0.05458999538792623507, -1.264741368075137817, 6.499999999999999112 ) ) ;
#13055=EDGE_CURVE ( 'NONE', #5825, #3667, #8843, .T. ) ;
#13108=CARTESIAN_POINT ( 'NONE',  ( 5.074999999999999289, 3.752776749732562589, 6.500000000000000000 ) ) ;
#13115=CARTESIAN_POINT ( 'NONE',  ( 0.000000000000000000, 0.000000000000000000, 0.000000000000000000 ) ) ;
#13128=CARTESIAN_POINT ( 'NONE',  ( 0.5805565836007702263, -7.505553499465148271, -1.692530754021427292E-16 ) ) ;
#13139=EDGE_CURVE ( 'NONE', #4779, #5825, #5052, .T. ) ;
#13150=VERTEX_POINT ( 'NONE', #12476 ) ;
#13196=EDGE_CURVE ( 'NONE', #13742, #15419, #8508, .T. ) ;
#13213=DIRECTION ( 'NONE',  ( 1.000000000000000000, 0.000000000000000000, 0.000000000000000000 ) ) ;
#13231=ORIENTED_EDGE ( 'NONE', *, *, #3594, .T. ) ;
#13235=DIRECTION ( 'NONE',  ( 1.000000000000000000, 0.000000000000000000, -0.000000000000000000 ) ) ;
#13292=ORIENTED_EDGE ( 'NONE', *, *, #6180, .F. ) ;
#13296=ORIENTED_EDGE ( 'NONE', *, *, #12118, .T. ) ;
#13311=ORIENTED_EDGE ( 'NONE', *, *, #13196, .T. ) ;
#13314=VERTEX_POINT ( 'NONE', #19281 ) ;
#13337=DIRECTION ( 'NONE',  ( 0.000000000000000000, 0.000000000000000000, -1.000000000000000000 ) ) ;
#13344=VERTEX_POINT ( 'NONE', #3166 ) ;
#13387=VECTOR ( 'NONE', #2105, 999.9999999999998863 ) ;
#13415=FACE_OUTER_BOUND ( 'NONE', #3174, .T. ) ;
#13445=CARTESIAN_POINT ( 'NONE',  ( 0.06682554136338024475, -4.993536075455418555, 4.350941807883115686 ) ) ;
#13491=CARTESIAN_POINT ( 'NONE',  ( 0.5805565836007702263, -7.505553499465148271, -1.692530754021427292E-16 ) ) ;
#13559=CARTESIAN_POINT ( 'NONE',  ( 0.000000000000000000, 0.000000000000000000, 0.000000000000000000 ) ) ;
#13562=EDGE_CURVE ( 'NONE', #20822, #5825, #11317, .T. ) ;
#13578=CARTESIAN_POINT ( 'NONE',  ( 0.000000000000000000, 0.000000000000000000, 0.000000000000000000 ) ) ;
#13622=PLANE ( 'NONE',  #9308 ) ;
#13659=CARTESIAN_POINT ( 'NONE',  ( 0.000000000000000000, 7.505553499465139389, 0.000000000000000000 ) ) ;
#13700=AXIS2_PLACEMENT_3D ( 'NONE', #9323, #19179, #2634 ) ;
#13706=LINE ( 'NONE', #1934, #21288 ) ;
#13742=VERTEX_POINT ( 'NONE', #19334 ) ;
#13749=VERTEX_POINT ( 'NONE', #7651 ) ;
#13790=ORIENTED_EDGE ( 'NONE', *, *, #16330, .F. ) ;
#13811=EDGE_CURVE ( 'NONE', #13749, #13314, #17269, .T. ) ;
#13825=PLANE ( 'NONE',  #16637 ) ;
#13835=( GEOMETRIC_REPRESENTATION_CONTEXT ( 3 ) GLOBAL_UNCERTAINTY_ASSIGNED_CONTEXT ( ( #1657 ) ) GLOBAL_UNIT_ASSIGNED_CONTEXT ( ( #14638, #9319, #16254 ) ) REPRESENTATION_CONTEXT ( 'NONE', 'WORKASPACE' ) );
#13849=EDGE_CURVE ( 'NONE', #12831, #2272, #15115, .T. ) ;
#13866=CARTESIAN_POINT ( 'NONE',  ( 0.000000000000000000, 0.000000000000000000, 0.000000000000000000 ) ) ;
#13931=DIRECTION ( 'NONE',  ( 0.000000000000000000, -1.000000000000000000, 0.000000000000000000 ) ) ;
#13934=B_SPLINE_CURVE_WITH_KNOTS ( 'NONE', 3,
 ( #7463, #15609, #12348, #15713, #5849, #17326 ),
 .UNSPECIFIED., .F., .F.,
 ( 4, 2, 4 ),
 ( 0.02294124189247800580, 0.02484059228080998452, 0.02673994266914196671 ),
 .UNSPECIFIED. ) ;
#14060=CARTESIAN_POINT ( 'NONE',  ( 5.674999999999999822, -7.505553499465148271, 0.000000000000000000 ) ) ;
#14070=EDGE_LOOP ( 'NONE', ( #19791, #933, #530, #17300, #8912, #4860 ) ) ;
#14150=VERTEX_POINT ( 'NONE', #14460 ) ;
#14176=ORIENTED_EDGE ( 'NONE', *, *, #9237, .F. ) ;
#14185=FACE_OUTER_BOUND ( 'NONE', #8658, .T. ) ;
#14227=ORIENTED_EDGE ( 'NONE', *, *, #17681, .F. ) ;
#14263=DIRECTION ( 'NONE',  ( 0.000000000000000000, -0.8660254037844381525, -0.5000000000000009992 ) ) ;
#14343=ORIENTED_EDGE ( 'NONE', *, *, #2217, .T. ) ;
#14356=DIRECTION ( 'NONE',  ( 0.000000000000000000, 0.000000000000000000, -1.000000000000000000 ) ) ;
#14362=ORIENTED_EDGE ( 'NONE', *, *, #3929, .F. ) ;
#14381=DIRECTION ( 'NONE',  ( -1.000000000000000000, 0.000000000000000000, -0.000000000000000000 ) ) ;
#14393=EDGE_LOOP ( 'NONE', ( #1418, #11967, #12601, #336, #11064, #16185 ) ) ;
#14439=EDGE_LOOP ( 'NONE', ( #4115, #13296, #13790, #21372 ) ) ;
#14442=DIRECTION ( 'NONE',  ( 0.000000000000000000, 0.000000000000000000, -1.000000000000000000 ) ) ;
#14460=CARTESIAN_POINT ( 'NONE',  ( 0.000000000000000000, 5.629165124598848102, 3.250000000000005329 ) ) ;
#14463=EDGE_LOOP ( 'NONE', ( #19136, #18252, #5952, #8560 ) ) ;
#14465=ORIENTED_EDGE ( 'NONE', *, *, #2217, .F. ) ;
#14515=CARTESIAN_POINT ( 'NONE',  ( 5.074999999999999289, 3.752776749732560368, -6.499999999999999112 ) ) ;
#14531=CARTESIAN_POINT ( 'NONE',  ( 5.074999999999999289, 3.752776749732560368, -6.499999999999999112 ) ) ;
#14539=CARTESIAN_POINT ( 'NONE',  ( 0.1061556211655316634, 4.836380039389415408, -4.623144047065555817 ) ) ;
#14568=EDGE_LOOP ( 'NONE', ( #15556, #14831, #2638 ) ) ;
#14575=EDGE_LOOP ( 'NONE', ( #20941, #7714, #18912 ) ) ;
#14626=LINE ( 'NONE', #14515, #20124 ) ;
#14636=FACE_OUTER_BOUND ( 'NONE', #9884, .T. ) ;
#14638=( LENGTH_UNIT ( ) NAMED_UNIT ( * ) SI_UNIT ( .MILLI., .METRE. ) );
#14688=PLANE ( 'NONE',  #1366 ) ;
#14736=B_SPLINE_CURVE_WITH_KNOTS ( 'NONE', 3,
 ( #304, #198, #16742, #10120, #8495, #15121, #6872, #13491 ),
 .UNSPECIFIED., .F., .F.,
 ( 4, 2, 2, 4 ),
 ( 0.003797433802554431564, 0.004743183970586230952, 0.005688934138618030774, 0.007580434474681628683 ),
 .UNSPECIFIED. ) ;
#14748=FACE_OUTER_BOUND ( 'NONE', #17638, .T. ) ;
#14771=FACE_OUTER_BOUND ( 'NONE', #14463, .T. ) ;
#14831=ORIENTED_EDGE ( 'NONE', *, *, #16099, .T. ) ;
#14848=DIRECTION ( 'NONE',  ( 0.000000000000000000, 0.000000000000000000, 1.000000000000000000 ) ) ;
#14849=EDGE_CURVE ( 'NONE', #5930, #21094, #9911, .T. ) ;
#14905=DIRECTION ( 'NONE',  ( -1.000000000000000000, -0.000000000000000000, -0.000000000000000000 ) ) ;
#14914=AXIS2_PLACEMENT_3D ( 'NONE', #11858, #415, #3323 ) ;
#14936=ORIENTED_EDGE ( 'NONE', *, *, #16714, .T. ) ;
#14939=CARTESIAN_POINT ( 'NONE',  ( 0.5805565836007647862, 7.505553499465139389, 2.227827669841787811E-16 ) ) ;
#14963=ORIENTED_EDGE ( 'NONE', *, *, #18010, .T. ) ;
#14978=PRODUCT_CONTEXT ( 'NONE', #16768, 'mechanical' ) ;
#15011=CARTESIAN_POINT ( 'NONE',  ( 0.5805565836007606784, -3.752776749732561701, 6.500000000000000000 ) ) ;
#15080=FACE_OUTER_BOUND ( 'NONE', #893, .T. ) ;
#15115=CIRCLE ( 'NONE', #261, 6.500000000000000888 ) ;
#15121=CARTESIAN_POINT ( 'NONE',  ( 0.2578475836320759385, -6.890627091270380866, -1.065083781909174299 ) ) ;
#15157=ORIENTED_EDGE ( 'NONE', *, *, #20596, .F. ) ;
#15180=PLANE ( 'NONE',  #2190 ) ;
#15206=( GEOMETRIC_REPRESENTATION_CONTEXT ( 3 ) GLOBAL_UNCERTAINTY_ASSIGNED_CONTEXT ( ( #7432 ) ) GLOBAL_UNIT_ASSIGNED_CONTEXT ( ( #16819, #386, #1571 ) ) REPRESENTATION_CONTEXT ( 'NONE', 'WORKASPACE' ) );
#15219=DIRECTION ( 'NONE',  ( -1.000000000000000000, -0.000000000000000000, -0.000000000000000000 ) ) ;
#15253=STYLED_ITEM('',(#21442),#4901);
#15258=CARTESIAN_POINT ( 'NONE',  ( 5.074999999999999289, 0.000000000000000000, 0.000000000000000000 ) ) ;
#15275=CARTESIAN_POINT ( 'NONE',  ( 5.074999999999999289, 6.500000000000000888, 0.000000000000000000 ) ) ;
#15290=EDGE_LOOP ( 'NONE', ( #12884, #17069, #3773 ) ) ;
#15306=B_SPLINE_CURVE_WITH_KNOTS ( 'NONE', 3,
 ( #9584, #9265, #15883, #1071, #12632, #7641 ),
 .UNSPECIFIED., .F., .F.,
 ( 4, 2, 4 ),
 ( 2.380733003144577723E-07, 0.001898835937927388726, 0.003797433802554463222 ),
 .UNSPECIFIED. ) ;
#15328=AXIS2_PLACEMENT_3D ( 'NONE', #13559, #18300, #3697 ) ;
#15419=VERTEX_POINT ( 'NONE', #20950 ) ;
#15450=DIRECTION ( 'NONE',  ( 0.000000000000000000, 0.000000000000000000, 1.000000000000000000 ) ) ;
#15478=EDGE_LOOP ( 'NONE', ( #7911, #19210, #3146 ) ) ;
#15488=FACE_OUTER_BOUND ( 'NONE', #2164, .T. ) ;
#15530=FACE_OUTER_BOUND ( 'NONE', #14393, .T. ) ;
#15556=ORIENTED_EDGE ( 'NONE', *, *, #8233, .T. ) ;
#15600=DIRECTION ( 'NONE',  ( 1.000000000000000000, 0.000000000000000000, 0.000000000000000000 ) ) ;
#15609=CARTESIAN_POINT ( 'NONE',  ( -3.697298814765020980E-16, -0.6346842323187746882, -6.500000000000000000 ) ) ;
#15618=DIRECTION ( 'NONE',  ( -1.000000000000000000, -0.000000000000000000, -0.000000000000000000 ) ) ;
#15698=DIRECTION ( 'NONE',  ( 1.000000000000000000, 0.000000000000000000, 0.000000000000000000 ) ) ;
#15702=DIRECTION ( 'NONE',  ( -1.000000000000000000, -0.000000000000000000, -0.000000000000000000 ) ) ;
#15713=CARTESIAN_POINT ( 'NONE',  ( 0.2565376335216141834, -2.516992571280034507, -6.499999999999999112 ) ) ;
#15739=ORIENTED_EDGE ( 'NONE', *, *, #8289, .T. ) ;
#15796=EDGE_LOOP ( 'NONE', ( #12517, #21150, #9234, #21044, #2748, #14227 ) ) ;
#15809=DIRECTION ( 'NONE',  ( 0.000000000000000000, 0.5000000000000004441, -0.8660254037844383745 ) ) ;
#15836=CARTESIAN_POINT ( 'NONE',  ( 0.5805565836007647862, 7.505553499465139389, 2.227827669841787811E-16 ) ) ;
#15873=ORIENTED_EDGE ( 'NONE', *, *, #2238, .T. ) ;
#15883=CARTESIAN_POINT ( 'NONE',  ( 0.2573354458087866448, -6.889406814520517841, 1.067197363239227759 ) ) ;
#15911=LINE ( 'NONE', #8973, #10268 ) ;
#15944=AXIS2_PLACEMENT_3D ( 'NONE', #8896, #3714, #12259 ) ;
#15973=DIRECTION ( 'NONE',  ( 1.000000000000000000, 0.000000000000000000, 0.000000000000000000 ) ) ;
#16001=ADVANCED_FACE ( 'NONE', ( #8038 ), #11290, .F. ) ;
#16036=VECTOR ( 'NONE', #15809, 1000.000000000000000 ) ;
#16066=ORIENTED_EDGE ( 'NONE', *, *, #17134, .F. ) ;
#16099=EDGE_CURVE ( 'NONE', #12049, #4779, #13014, .T. ) ;
#16125=DIRECTION ( 'NONE',  ( 0.000000000000000000, 0.000000000000000000, 1.000000000000000000 ) ) ;
#16126=AXIS2_PLACEMENT_3D ( 'NONE', #19231, #17499, #10892 ) ;
#16185=ORIENTED_EDGE ( 'NONE', *, *, #12661, .F. ) ;
#16254=( NAMED_UNIT ( * ) SI_UNIT ( $, .STERADIAN. ) SOLID_ANGLE_UNIT ( ) );
#16259=CARTESIAN_POINT ( 'NONE',  ( 0.06682554136337909290, 6.264794173742276762, 2.149058192116895860 ) ) ;
#16260=CARTESIAN_POINT ( 'NONE',  ( -1.456896669277397076E-16, 0.6351314446025495553, -6.500000000000000000 ) ) ;
#16307=FACE_OUTER_BOUND ( 'NONE', #5249, .T. ) ;
#16330=EDGE_CURVE ( 'NONE', #5058, #19703, #20971, .T. ) ;
#16344=DIRECTION ( 'NONE',  ( 0.000000000000000000, 0.000000000000000000, 1.000000000000000000 ) ) ;
#16371=EDGE_CURVE ( 'NONE', #13150, #18908, #12037, .T. ) ;
#16415=DIRECTION ( 'NONE',  ( 0.000000000000000000, 0.000000000000000000, -1.000000000000000000 ) ) ;
#16444=CARTESIAN_POINT ( 'NONE',  ( 45.67500000000000426, 0.000000000000000000, 3.309499999999999886 ) ) ;
#16454=EDGE_LOOP ( 'NONE', ( #15739, #3671, #5310 ) ) ;
#16474=DIRECTION ( 'NONE',  ( 0.000000000000000000, 0.000000000000000000, -1.000000000000000000 ) ) ;
#16482=VERTEX_POINT ( 'NONE', #10838 ) ;
#16522=CARTESIAN_POINT ( 'NONE',  ( 5.074999999999999289, 6.500000000000000888, 0.000000000000000000 ) ) ;
#16573=FACE_OUTER_BOUND ( 'NONE', #15478, .T. ) ;
#16606=B_SPLINE_CURVE_WITH_KNOTS ( 'NONE', 3,
 ( #5594, #18172, #7314, #18574, #3370, #12197 ),
 .UNSPECIFIED., .F., .F.,
 ( 4, 2, 4 ),
 ( 2.380733003139562229E-07, 0.001898835937927375282, 0.003797433802554436334 ),
 .UNSPECIFIED. ) ;
#16626=VECTOR ( 'NONE', #20921, 999.9999999999998863 ) ;
#16637=AXIS2_PLACEMENT_3D ( 'NONE', #4187, #14263, #4403 ) ;
#16705=ADVANCED_BREP_SHAPE_REPRESENTATION ( '', ( #4901, #12794 ), #13835 ) ;
#16714=EDGE_CURVE ( 'NONE', #7492, #10771, #3164, .T. ) ;
#16736=CIRCLE ( 'NONE', #17418, 4.000000000000000000 ) ;
#16742=CARTESIAN_POINT ( 'NONE',  ( 0.01372220897662189062, -5.948365447239590154, -2.697128823393882158 ) ) ;
#16768=APPLICATION_CONTEXT ( 'automotive_design' ) ;
#16777=EDGE_LOOP ( 'NONE', ( #6270, #15157 ) ) ;
#16800=CARTESIAN_POINT ( 'NONE',  ( 0.5805565836007606784, -3.752776749732561701, 6.500000000000000000 ) ) ;
#16819=( LENGTH_UNIT ( ) NAMED_UNIT ( * ) SI_UNIT ( .MILLI., .METRE. ) );
#16827=CONICAL_SURFACE ( 'NONE', #13000, 6.500000000000000000, 1.047197551196600296 ) ;
#16845=AXIS2_PLACEMENT_3D ( 'NONE', #3191, #17996, #6315 ) ;
#16876=CARTESIAN_POINT ( 'NONE',  ( -4.646822748637091660E-15, 5.948846446048900560, -2.696295709017756614 ) ) ;
#16949=DIRECTION ( 'NONE',  ( 0.000000000000000000, -0.5000000000000018874, -0.8660254037844375974 ) ) ;
#17011=PLANE ( 'NONE',  #20536 ) ;
#17030=ADVANCED_FACE ( 'NONE', ( #2605 ), #619, .T. ) ;
#17064=VECTOR ( 'NONE', #13931, 1000.000000000000000 ) ;
#17068=AXIS2_PLACEMENT_3D ( 'NONE', #12656, #4433, #20743 ) ;
#17069=ORIENTED_EDGE ( 'NONE', *, *, #9361, .T. ) ;
#17096=B_SPLINE_CURVE_WITH_KNOTS ( 'NONE', 3,
 ( #367, #3389, #5214, #13445, #8345, #8453, #8559, #16800 ),
 .UNSPECIFIED., .F., .F.,
 ( 4, 2, 2, 4 ),
 ( 0.003797433802554463222, 0.004743183970586255238, 0.005688934138618048121, 0.007580434474681636489 ),
 .UNSPECIFIED. ) ;
#17134=EDGE_CURVE ( 'NONE', #5669, #5772, #15911, .T. ) ;
#17136=CARTESIAN_POINT ( 'NONE',  ( 44.98449999999999704, 0.000000000000000000, 4.000000000000000000 ) ) ;
#17172=ORIENTED_EDGE ( 'NONE', *, *, #6348, .T. ) ;
#17223=DIRECTION ( 'NONE',  ( -0.7071067811865530128, 0.000000000000000000, 0.7071067811865421326 ) ) ;
#17234=LINE ( 'NONE', #20580, #4801 ) ;
#17269=B_SPLINE_CURVE_WITH_KNOTS ( 'NONE', 3,
 ( #1387, #4415, #17607, #2798, #9384, #6135 ),
 .UNSPECIFIED., .F., .F.,
 ( 4, 2, 4 ),
 ( 0.01067228060976418112, 0.01257272967502433281, 0.01447317874028448276 ),
 .UNSPECIFIED. ) ;
#17300=ORIENTED_EDGE ( 'NONE', *, *, #7946, .F. ) ;
#17302=DIRECTION ( 'NONE',  ( 1.000000000000000000, 0.000000000000000000, -0.000000000000000000 ) ) ;
#17316=DIRECTION ( 'NONE',  ( 0.000000000000000000, 0.000000000000000000, 1.000000000000000000 ) ) ;
#17323=CARTESIAN_POINT ( 'NONE',  ( 0.000000000000000000, 0.000000000000000000, 4.000000000000000000 ) ) ;
#17326=CARTESIAN_POINT ( 'NONE',  ( 0.5805565836007647862, -3.752776749732576356, -6.500000000000000000 ) ) ;
#17410=ORIENTED_EDGE ( 'NONE', *, *, #2578, .F. ) ;
#17418=AXIS2_PLACEMENT_3D ( 'NONE', #17839, #6369, #16344 ) ;
#17499=DIRECTION ( 'NONE',  ( 1.000000000000000000, 0.000000000000000000, -0.000000000000000000 ) ) ;
#17506=AXIS2_PLACEMENT_3D ( 'NONE', #6743, #1463, #19842 ) ;
#17514=EDGE_CURVE ( 'NONE', #6352, #13150, #6467, .T. ) ;
#17521=CARTESIAN_POINT ( 'NONE',  ( 5.074999999999999289, 6.500000000000000888, 0.000000000000000000 ) ) ;
#17563=AXIS2_PLACEMENT_3D ( 'NONE', #12938, #2884, #19419 ) ;
#17607=CARTESIAN_POINT ( 'NONE',  ( 0.05613245601076813363, 1.278525034532179916, 6.500000000000000888 ) ) ;
#17638=EDGE_LOOP ( 'NONE', ( #20875, #18881, #11891 ) ) ;
#17658=DIRECTION ( 'NONE',  ( 1.000000000000000000, 0.000000000000000000, -0.000000000000000000 ) ) ;
#17665=CARTESIAN_POINT ( 'NONE',  ( -4.707244432207906043E-15, 5.469921996229797578, -3.525817189091414949 ) ) ;
#17681=EDGE_CURVE ( 'NONE', #3667, #14150, #11625, .T. ) ;
#17742=AXIS2_PLACEMENT_3D ( 'NONE', #1238, #21022, #14442 ) ;
#17758=LINE ( 'NONE', #13108, #8939 ) ;
#17813=ADVANCED_FACE ( 'NONE', ( #11541 ), #11321, .F. ) ;
#17817=CARTESIAN_POINT ( 'NONE',  ( 0.5805565836007647862, -3.752776749732576356, -6.500000000000000000 ) ) ;
#17823=VERTEX_POINT ( 'NONE', #17817 ) ;
#17839=CARTESIAN_POINT ( 'NONE',  ( 44.98449999999999704, 0.000000000000000000, 0.000000000000000000 ) ) ;
#17861=CARTESIAN_POINT ( 'NONE',  ( 0.000000000000000000, 5.629165124598848102, 3.250000000000005329 ) ) ;
#17897=EDGE_LOOP ( 'NONE', ( #12433, #15873, #17172, #18484 ) ) ;
#17996=DIRECTION ( 'NONE',  ( -1.000000000000000000, 0.000000000000000000, -0.000000000000000000 ) ) ;
#18005=FACE_OUTER_BOUND ( 'NONE', #3361, .T. ) ;
#18010=EDGE_CURVE ( 'NONE', #13344, #6352, #13706, .T. ) ;
#18011=AXIS2_PLACEMENT_3D ( 'NONE', #6590, #13213, #1421 ) ;
#18076=DIRECTION ( 'NONE',  ( -1.000000000000000000, -0.000000000000000000, -0.000000000000000000 ) ) ;
#18079=CARTESIAN_POINT ( 'NONE',  ( 0.000000000000000000, 0.000000000000000000, 0.000000000000000000 ) ) ;
#18115=ORIENTED_EDGE ( 'NONE', *, *, #9361, .F. ) ;
#18151=EDGE_CURVE ( 'NONE', #4289, #11401, #2556, .T. ) ;
#18165=DIRECTION ( 'NONE',  ( -0.000000000000000000, 1.000000000000000000, 1.155626614413199331E-16 ) ) ;
#18172=CARTESIAN_POINT ( 'NONE',  ( 0.4033376246892473871, 4.059728990630799395, 5.968343123267132455 ) ) ;
#18180=CONICAL_SURFACE ( 'NONE', #8847, 6.500000000000000000, 1.047197551196600296 ) ;
#18183=CARTESIAN_POINT ( 'NONE',  ( 0.2595206531158515961, 2.531175536751804955, -6.499999999999999112 ) ) ;
#18214=EDGE_CURVE ( 'NONE', #5669, #13344, #19558, .T. ) ;
#18252=ORIENTED_EDGE ( 'NONE', *, *, #3102, .T. ) ;
#18257=DIRECTION ( 'NONE',  ( 0.000000000000000000, -1.155626614413199331E-16, 1.000000000000000000 ) ) ;
#18270=CARTESIAN_POINT ( 'NONE',  ( 0.4033376246892497741, 7.198601258566900363, -0.5316568767328673228 ) ) ;
#18300=DIRECTION ( 'NONE',  ( -1.000000000000000000, -0.000000000000000000, -0.000000000000000000 ) ) ;
#18334=ADVANCED_FACE ( 'NONE', ( #14748 ), #16827, .T. ) ;
#18430=ADVANCED_FACE ( 'NONE', ( #8337 ), #18180, .T. ) ;
#18444=EDGE_LOOP ( 'NONE', ( #16066, #4401, #14963, #8263, #3278, #17410 ) ) ;
#18471=FACE_OUTER_BOUND ( 'NONE', #3459, .T. ) ;
#18484=ORIENTED_EDGE ( 'NONE', *, *, #13196, .F. ) ;
#18547=AXIS2_PLACEMENT_3D ( 'NONE', #4054, #15219, #721 ) ;
#18574=CARTESIAN_POINT ( 'NONE',  ( 0.05533025579362052526, 4.993776679985852951, 4.350525068611870161 ) ) ;
#18583=CIRCLE ( 'NONE', #4783, 6.500000000000000888 ) ;
#18655=ADVANCED_FACE ( 'NONE', ( #15488 ), #4597, .T. ) ;
#18685=VECTOR ( 'NONE', #16949, 999.9999999999998863 ) ;
#18689=DIRECTION ( 'NONE',  ( -1.000000000000000000, -0.000000000000000000, -0.000000000000000000 ) ) ;
#18822=ORIENTED_EDGE ( 'NONE', *, *, #8780, .T. ) ;
#18867=ADVANCED_FACE ( 'NONE', ( #6367 ), #6263, .T. ) ;
#18879=B_SPLINE_CURVE_WITH_KNOTS ( 'NONE', 3,
 ( #20915, #17665, #8123, #4474, #14539, #9441, #7708, #21340 ),
 .UNSPECIFIED., .F., .F.,
 ( 4, 2, 2, 4 ),
 ( 0.003797433802554451947, 0.004743183970586247432, 0.005688934138618042050, 0.007580434474681631285 ),
 .UNSPECIFIED. ) ;
#18881=ORIENTED_EDGE ( 'NONE', *, *, #13562, .T. ) ;
#18908=VERTEX_POINT ( 'NONE', #1411 ) ;
#18912=ORIENTED_EDGE ( 'NONE', *, *, #5721, .T. ) ;
#18923=CARTESIAN_POINT ( 'NONE',  ( 45.67500000000000426, 0.000000000000000000, 0.000000000000000000 ) ) ;
#18999=ORIENTED_EDGE ( 'NONE', *, *, #20596, .T. ) ;
#19020=DIRECTION ( 'NONE',  ( 0.000000000000000000, 0.000000000000000000, 1.000000000000000000 ) ) ;
#19040=LINE ( 'NONE', #4224, #16036 ) ;
#19042=DIRECTION ( 'NONE',  ( -1.000000000000000000, -0.000000000000000000, -0.000000000000000000 ) ) ;
#19107=ORIENTED_EDGE ( 'NONE', *, *, #958, .T. ) ;
#19136=ORIENTED_EDGE ( 'NONE', *, *, #16330, .T. ) ;
#19137=DIRECTION ( 'NONE',  ( 0.000000000000000000, 0.000000000000000000, -1.000000000000000000 ) ) ;
#19179=DIRECTION ( 'NONE',  ( -1.000000000000000000, -0.000000000000000000, 0.000000000000000000 ) ) ;
#19201=ADVANCED_FACE ( 'NONE', ( #1593 ), #19752, .T. ) ;
#19210=ORIENTED_EDGE ( 'NONE', *, *, #19579, .T. ) ;
#19226=CARTESIAN_POINT ( 'NONE',  ( 5.074999999999999289, -7.505553499465148271, 0.000000000000000000 ) ) ;
#19231=CARTESIAN_POINT ( 'NONE',  ( 0.000000000000000000, 0.000000000000000000, 0.000000000000000000 ) ) ;
#19254=DIRECTION ( 'NONE',  ( -0.000000000000000000, 1.000000000000000000, 1.155626614413199331E-16 ) ) ;
#19281=CARTESIAN_POINT ( 'NONE',  ( 0.5805565836007611225, 3.752776749732563033, 6.500000000000000000 ) ) ;
#19288=ORIENTED_EDGE ( 'NONE', *, *, #18214, .T. ) ;
#19334=CARTESIAN_POINT ( 'NONE',  ( 5.674999999999999822, 4.898587196589412829E-16, -4.000000000000000000 ) ) ;
#19345=CARTESIAN_POINT ( 'NONE',  ( 5.674999999999999822, 0.000000000000000000, 0.000000000000000000 ) ) ;
#19419=DIRECTION ( 'NONE',  ( 0.000000000000000000, 0.000000000000000000, -1.000000000000000000 ) ) ;
#19558=CIRCLE ( 'NONE', #20959, 6.500000000000000888 ) ;
#19564=AXIS2_PLACEMENT_3D ( 'NONE', #10514, #10301, #20168 ) ;
#19570=DIRECTION ( 'NONE',  ( 0.000000000000000000, 0.5000000000000004441, -0.8660254037844383745 ) ) ;
#19579=EDGE_CURVE ( 'NONE', #7492, #13150, #10860, .T. ) ;
#19596=DIRECTION ( 'NONE',  ( 1.000000000000000000, 0.000000000000000000, -0.000000000000000000 ) ) ;
#19703=VERTEX_POINT ( 'NONE', #3077 ) ;
#19752=PLANE ( 'NONE',  #9436 ) ;
#19791=ORIENTED_EDGE ( 'NONE', *, *, #18214, .F. ) ;
#19802=DIRECTION ( 'NONE',  ( 0.000000000000000000, 0.000000000000000000, 1.000000000000000000 ) ) ;
#19815=CARTESIAN_POINT ( 'NONE',  ( 0.5805565836007597902, 3.752776749732560368, -6.499999999999999112 ) ) ;
#19842=DIRECTION ( 'NONE',  ( 0.000000000000000000, 0.000000000000000000, -1.000000000000000000 ) ) ;
#19865=LINE ( 'NONE', #11642, #6346 ) ;
#19887=FACE_OUTER_BOUND ( 'NONE', #14568, .T. ) ;
#19916=CARTESIAN_POINT ( 'NONE',  ( 5.674999999999999822, 7.505553499465139389, 0.000000000000000000 ) ) ;
#19918=CARTESIAN_POINT ( 'NONE',  ( 0.05613245601036562227, 1.278525034529254034, -6.499999999999999112 ) ) ;
#19970=CARTESIAN_POINT ( 'NONE',  ( 0.000000000000000000, 0.000000000000000000, 6.500000000000000000 ) ) ;
#20006=DIRECTION ( 'NONE',  ( 0.000000000000000000, -0.8660254037844380415, 0.5000000000000011102 ) ) ;
#20124=VECTOR ( 'NONE', #18165, 1000.000000000000000 ) ;
#20167=DIRECTION ( 'NONE',  ( -1.000000000000000000, -0.000000000000000000, -0.000000000000000000 ) ) ;
#20168=DIRECTION ( 'NONE',  ( 0.000000000000000000, 0.000000000000000000, -1.000000000000000000 ) ) ;
#20182=CIRCLE ( 'NONE', #2952, 6.500000000000000888 ) ;
#20200=EDGE_CURVE ( 'NONE', #12831, #5170, #19040, .T. ) ;
#20203=CARTESIAN_POINT ( 'NONE',  ( 0.000000000000000000, 0.000000000000000000, 0.000000000000000000 ) ) ;
#20210=ADVANCED_FACE ( 'NONE', ( #14185 ), #1185, .T. ) ;
#20217=DIRECTION ( 'NONE',  ( -1.000000000000000000, -0.000000000000000000, -0.000000000000000000 ) ) ;
#20524=EDGE_CURVE ( 'NONE', #17823, #4779, #1490, .T. ) ;
#20536=AXIS2_PLACEMENT_3D ( 'NONE', #3492, #10077, #6938 ) ;
#20556=FACE_OUTER_BOUND ( 'NONE', #11889, .T. ) ;
#20569=ORIENTED_EDGE ( 'NONE', *, *, #13811, .F. ) ;
#20580=CARTESIAN_POINT ( 'NONE',  ( 5.674999999999999822, -3.752776749732561257, 6.500000000000000000 ) ) ;
#20596=EDGE_CURVE ( 'NONE', #21094, #5930, #20832, .T. ) ;
#20627=FACE_OUTER_BOUND ( 'NONE', #2191, .T. ) ;
#20743=DIRECTION ( 'NONE',  ( 0.000000000000000000, 0.000000000000000000, -1.000000000000000000 ) ) ;
#20822=VERTEX_POINT ( 'NONE', #2236 ) ;
#20832=CIRCLE ( 'NONE', #4918, 3.309499999999999886 ) ;
#20834=CARTESIAN_POINT ( 'NONE',  ( 5.074999999999999289, 3.752776749732560368, -6.499999999999999112 ) ) ;
#20843=VECTOR ( 'NONE', #2507, 1000.000000000000000 ) ;
#20868=LINE ( 'NONE', #14060, #1884 ) ;
#20870=PLANE ( 'NONE',  #4271 ) ;
#20875=ORIENTED_EDGE ( 'NONE', *, *, #6033, .T. ) ;
#20909=EDGE_CURVE ( 'NONE', #18908, #13314, #2549, .T. ) ;
#20915=CARTESIAN_POINT ( 'NONE',  ( 0.000000000000000000, 5.629165124598846326, -3.250000000000007550 ) ) ;
#20921=DIRECTION ( 'NONE',  ( -0.7071067811865530128, 8.659560562354868763E-17, -0.7071067811865421326 ) ) ;
#20941=ORIENTED_EDGE ( 'NONE', *, *, #18151, .T. ) ;
#20943=EDGE_LOOP ( 'NONE', ( #4144, #9253, #13292 ) ) ;
#20950=CARTESIAN_POINT ( 'NONE',  ( 5.674999999999999822, 0.000000000000000000, 4.000000000000000000 ) ) ;
#20959=AXIS2_PLACEMENT_3D ( 'NONE', #4285, #19596, #16474 ) ;
#20971=CIRCLE ( 'NONE', #10590, 4.000000000000000000 ) ;
#21022=DIRECTION ( 'NONE',  ( -1.000000000000000000, -0.000000000000000000, 0.000000000000000000 ) ) ;
#21044=ORIENTED_EDGE ( 'NONE', *, *, #12063, .F. ) ;
#21066=DIRECTION ( 'NONE',  ( -1.000000000000000000, -0.000000000000000000, -0.000000000000000000 ) ) ;
#21094=VERTEX_POINT ( 'NONE', #9767 ) ;
#21150=ORIENTED_EDGE ( 'NONE', *, *, #13139, .F. ) ;
#21163=PRODUCT_DEFINITION_SHAPE ( 'NONE', 'NONE',  #48 ) ;
#21180=DIRECTION ( 'NONE',  ( 1.000000000000000000, 0.000000000000000000, 0.000000000000000000 ) ) ;
#21223=SHAPE_REPRESENTATION_RELATIONSHIP ( 'NONE' , 'NONE' ,  #8616, #16705 ) ;
#21265=CARTESIAN_POINT ( 'NONE',  ( 5.674999999999999822, -3.752776749732576356, -6.500000000000000000 ) ) ;
#21288=VECTOR ( 'NONE', #5158, 1000.000000000000000 ) ;
#21306=ORIENTED_EDGE ( 'NONE', *, *, #3594, .F. ) ;
#21340=CARTESIAN_POINT ( 'NONE',  ( 0.5805565836007597902, 3.752776749732560368, -6.499999999999999112 ) ) ;
#21372=ORIENTED_EDGE ( 'NONE', *, *, #3622, .F. ) ;
#21379=CARTESIAN_POINT ( 'NONE',  ( 0.5805565836007647862, -3.752776749732576356, -6.500000000000000000 ) ) ;
#21436=COLOUR_RGB('Black',0.12,0.14,0.17);
#21437=FILL_AREA_STYLE_COLOUR('',#21436);
#21438=FILL_AREA_STYLE('',(#21437));
#21439=SURFACE_STYLE_FILL_AREA(#21438);
#21440=SURFACE_SIDE_STYLE('',(#21439));
#21441=SURFACE_STYLE_USAGE(.BOTH.,#21440);
#21442=PRESENTATION_STYLE_ASSIGNMENT((#21441));
ENDSEC;
END-ISO-10303-21;
